ISO-10303-21;
HEADER;
/* Generated by software containing ST-Developer
 * from STEP Tools, Inc. (www.steptools.com) 
 */

FILE_DESCRIPTION(
/* description */ ('STEP AP214'),
/* implementation_level */ '2;1');

FILE_NAME(
/* name */ 'Ball Screw Support Spacer.step',
/* time_stamp */ '2026-11-15T14:49:54-08:00',
/* author */ (''),
/* organization */ (''),
/* preprocessor_version */ 'ST-DEVELOPER v20.2',
/* originating_system */ 'Autodesk Translation Framework v15.17.0.0',
/* authorisation */ '');

FILE_SCHEMA (('AUTOMOTIVE_DESIGN { 1 0 10303 214 3 1 1 }'));
ENDSEC;

DATA;
#10=MECHANICAL_DESIGN_GEOMETRIC_PRESENTATION_REPRESENTATION('',(#1103),#66721);
#1041=SHAPE_REPRESENTATION_RELATIONSHIP('SRR','None',#66898,#1072);
#1072=ADVANCED_BREP_SHAPE_REPRESENTATION('',(#1138),#66689);
#1103=STYLED_ITEM('',(#67095),#1138);
#1138=MANIFOLD_SOLID_BREP('Body1',#25669);
#1235=FACE_BOUND('',#3871,.T.);
#1236=FACE_BOUND('',#3872,.T.);
#1237=FACE_BOUND('',#3873,.T.);
#1238=FACE_BOUND('',#3874,.T.);
#1239=FACE_BOUND('',#3875,.T.);
#1240=FACE_BOUND('',#3876,.T.);
#1241=FACE_BOUND('',#3878,.T.);
#1242=FACE_BOUND('',#3879,.T.);
#1243=FACE_BOUND('',#3880,.T.);
#1244=FACE_BOUND('',#3881,.T.);
#1245=FACE_BOUND('',#3882,.T.);
#1246=FACE_BOUND('',#3883,.T.);
#1545=PLANE('',#26222);
#1546=PLANE('',#26223);
#1547=PLANE('',#26224);
#1548=PLANE('',#26225);
#1549=PLANE('',#26226);
#1550=PLANE('',#26227);
#2351=FACE_OUTER_BOUND('',#3860,.T.);
#2352=FACE_OUTER_BOUND('',#3861,.T.);
#2353=FACE_OUTER_BOUND('',#3862,.T.);
#2354=FACE_OUTER_BOUND('',#3863,.T.);
#2355=FACE_OUTER_BOUND('',#3864,.T.);
#2356=FACE_OUTER_BOUND('',#3865,.T.);
#2357=FACE_OUTER_BOUND('',#3866,.T.);
#2358=FACE_OUTER_BOUND('',#3867,.T.);
#2359=FACE_OUTER_BOUND('',#3868,.T.);
#2360=FACE_OUTER_BOUND('',#3869,.T.);
#2361=FACE_OUTER_BOUND('',#3870,.T.);
#2362=FACE_OUTER_BOUND('',#3877,.T.);
#3860=EDGE_LOOP('',(#17008,#17009,#17010,#17011));
#3861=EDGE_LOOP('',(#17012,#17013,#17014,#17015));
#3862=EDGE_LOOP('',(#17016,#17017,#17018,#17019));
#3863=EDGE_LOOP('',(#17020,#17021,#17022,#17023));
#3864=EDGE_LOOP('',(#17024,#17025,#17026,#17027));
#3865=EDGE_LOOP('',(#17028,#17029,#17030,#17031));
#3866=EDGE_LOOP('',(#17032,#17033,#17034,#17035));
#3867=EDGE_LOOP('',(#17036,#17037,#17038,#17039));
#3868=EDGE_LOOP('',(#17040,#17041,#17042,#17043));
#3869=EDGE_LOOP('',(#17044,#17045,#17046,#17047));
#3870=EDGE_LOOP('',(#17048,#17049,#17050,#17051));
#3871=EDGE_LOOP('',(#17052));
#3872=EDGE_LOOP('',(#17053));
#3873=EDGE_LOOP('',(#17054));
#3874=EDGE_LOOP('',(#17055));
#3875=EDGE_LOOP('',(#17056));
#3876=EDGE_LOOP('',(#17057));
#3877=EDGE_LOOP('',(#17058,#17059,#17060,#17061));
#3878=EDGE_LOOP('',(#17062));
#3879=EDGE_LOOP('',(#17063));
#3880=EDGE_LOOP('',(#17064));
#3881=EDGE_LOOP('',(#17065));
#3882=EDGE_LOOP('',(#17066));
#3883=EDGE_LOOP('',(#17067));
#5620=LINE('',#36617,#7609);
#5621=LINE('',#36623,#7610);
#5622=LINE('',#36629,#7611);
#5623=LINE('',#36635,#7612);
#5624=LINE('',#36641,#7613);
#5625=LINE('',#36647,#7614);
#5626=LINE('',#36652,#7615);
#5627=LINE('',#36654,#7616);
#5628=LINE('',#36656,#7617);
#5629=LINE('',#36657,#7618);
#5630=LINE('',#36660,#7619);
#5631=LINE('',#36662,#7620);
#5632=LINE('',#36663,#7621);
#5633=LINE('',#36666,#7622);
#5634=LINE('',#36668,#7623);
#5635=LINE('',#36669,#7624);
#5636=LINE('',#36671,#7625);
#5637=LINE('',#36672,#7626);
#7609=VECTOR('',#29223,3.3);
#7610=VECTOR('',#29230,3.3);
#7611=VECTOR('',#29237,3.3);
#7612=VECTOR('',#29244,3.3);
#7613=VECTOR('',#29251,3.3);
#7614=VECTOR('',#29258,3.3);
#7615=VECTOR('',#29263,1000.);
#7616=VECTOR('',#29264,1000.);
#7617=VECTOR('',#29265,1000.);
#7618=VECTOR('',#29266,1000.);
#7619=VECTOR('',#29269,1000.);
#7620=VECTOR('',#29270,1000.);
#7621=VECTOR('',#29271,1000.);
#7622=VECTOR('',#29274,1000.);
#7623=VECTOR('',#29275,1000.);
#7624=VECTOR('',#29276,1000.);
#7625=VECTOR('',#29279,1000.);
#7626=VECTOR('',#29280,1000.);
#9531=CIRCLE('',#26205,3.3);
#9532=CIRCLE('',#26206,3.3);
#9533=CIRCLE('',#26208,3.3);
#9534=CIRCLE('',#26209,3.3);
#9535=CIRCLE('',#26211,3.3);
#9536=CIRCLE('',#26212,3.3);
#9537=CIRCLE('',#26214,3.3);
#9538=CIRCLE('',#26215,3.3);
#9539=CIRCLE('',#26217,3.3);
#9540=CIRCLE('',#26218,3.3);
#9541=CIRCLE('',#26220,3.3);
#9542=CIRCLE('',#26221,3.3);
#10776=VERTEX_POINT('',#36614);
#10777=VERTEX_POINT('',#36616);
#10778=VERTEX_POINT('',#36620);
#10779=VERTEX_POINT('',#36622);
#10780=VERTEX_POINT('',#36626);
#10781=VERTEX_POINT('',#36628);
#10782=VERTEX_POINT('',#36632);
#10783=VERTEX_POINT('',#36634);
#10784=VERTEX_POINT('',#36638);
#10785=VERTEX_POINT('',#36640);
#10786=VERTEX_POINT('',#36644);
#10787=VERTEX_POINT('',#36646);
#10788=VERTEX_POINT('',#36650);
#10789=VERTEX_POINT('',#36651);
#10790=VERTEX_POINT('',#36653);
#10791=VERTEX_POINT('',#36655);
#10792=VERTEX_POINT('',#36659);
#10793=VERTEX_POINT('',#36661);
#10794=VERTEX_POINT('',#36665);
#10795=VERTEX_POINT('',#36667);
#13197=EDGE_CURVE('',#10776,#10776,#9531,.T.);
#13198=EDGE_CURVE('',#10776,#10777,#5620,.T.);
#13199=EDGE_CURVE('',#10777,#10777,#9532,.T.);
#13200=EDGE_CURVE('',#10778,#10778,#9533,.T.);
#13201=EDGE_CURVE('',#10778,#10779,#5621,.T.);
#13202=EDGE_CURVE('',#10779,#10779,#9534,.T.);
#13203=EDGE_CURVE('',#10780,#10780,#9535,.T.);
#13204=EDGE_CURVE('',#10780,#10781,#5622,.T.);
#13205=EDGE_CURVE('',#10781,#10781,#9536,.T.);
#13206=EDGE_CURVE('',#10782,#10782,#9537,.T.);
#13207=EDGE_CURVE('',#10782,#10783,#5623,.T.);
#13208=EDGE_CURVE('',#10783,#10783,#9538,.T.);
#13209=EDGE_CURVE('',#10784,#10784,#9539,.T.);
#13210=EDGE_CURVE('',#10784,#10785,#5624,.T.);
#13211=EDGE_CURVE('',#10785,#10785,#9540,.T.);
#13212=EDGE_CURVE('',#10786,#10786,#9541,.T.);
#13213=EDGE_CURVE('',#10786,#10787,#5625,.T.);
#13214=EDGE_CURVE('',#10787,#10787,#9542,.T.);
#13215=EDGE_CURVE('',#10788,#10789,#5626,.T.);
#13216=EDGE_CURVE('',#10790,#10789,#5627,.T.);
#13217=EDGE_CURVE('',#10791,#10790,#5628,.T.);
#13218=EDGE_CURVE('',#10791,#10788,#5629,.T.);
#13219=EDGE_CURVE('',#10789,#10792,#5630,.T.);
#13220=EDGE_CURVE('',#10793,#10792,#5631,.T.);
#13221=EDGE_CURVE('',#10790,#10793,#5632,.T.);
#13222=EDGE_CURVE('',#10792,#10794,#5633,.T.);
#13223=EDGE_CURVE('',#10795,#10794,#5634,.T.);
#13224=EDGE_CURVE('',#10793,#10795,#5635,.T.);
#13225=EDGE_CURVE('',#10794,#10788,#5636,.T.);
#13226=EDGE_CURVE('',#10795,#10791,#5637,.T.);
#17008=ORIENTED_EDGE('',*,*,#13197,.F.);
#17009=ORIENTED_EDGE('',*,*,#13198,.T.);
#17010=ORIENTED_EDGE('',*,*,#13199,.T.);
#17011=ORIENTED_EDGE('',*,*,#13198,.F.);
#17012=ORIENTED_EDGE('',*,*,#13200,.F.);
#17013=ORIENTED_EDGE('',*,*,#13201,.T.);
#17014=ORIENTED_EDGE('',*,*,#13202,.T.);
#17015=ORIENTED_EDGE('',*,*,#13201,.F.);
#17016=ORIENTED_EDGE('',*,*,#13203,.F.);
#17017=ORIENTED_EDGE('',*,*,#13204,.T.);
#17018=ORIENTED_EDGE('',*,*,#13205,.T.);
#17019=ORIENTED_EDGE('',*,*,#13204,.F.);
#17020=ORIENTED_EDGE('',*,*,#13206,.F.);
#17021=ORIENTED_EDGE('',*,*,#13207,.T.);
#17022=ORIENTED_EDGE('',*,*,#13208,.T.);
#17023=ORIENTED_EDGE('',*,*,#13207,.F.);
#17024=ORIENTED_EDGE('',*,*,#13209,.F.);
#17025=ORIENTED_EDGE('',*,*,#13210,.T.);
#17026=ORIENTED_EDGE('',*,*,#13211,.T.);
#17027=ORIENTED_EDGE('',*,*,#13210,.F.);
#17028=ORIENTED_EDGE('',*,*,#13212,.F.);
#17029=ORIENTED_EDGE('',*,*,#13213,.T.);
#17030=ORIENTED_EDGE('',*,*,#13214,.T.);
#17031=ORIENTED_EDGE('',*,*,#13213,.F.);
#17032=ORIENTED_EDGE('',*,*,#13215,.T.);
#17033=ORIENTED_EDGE('',*,*,#13216,.F.);
#17034=ORIENTED_EDGE('',*,*,#13217,.F.);
#17035=ORIENTED_EDGE('',*,*,#13218,.T.);
#17036=ORIENTED_EDGE('',*,*,#13219,.T.);
#17037=ORIENTED_EDGE('',*,*,#13220,.F.);
#17038=ORIENTED_EDGE('',*,*,#13221,.F.);
#17039=ORIENTED_EDGE('',*,*,#13216,.T.);
#17040=ORIENTED_EDGE('',*,*,#13222,.T.);
#17041=ORIENTED_EDGE('',*,*,#13223,.F.);
#17042=ORIENTED_EDGE('',*,*,#13224,.F.);
#17043=ORIENTED_EDGE('',*,*,#13220,.T.);
#17044=ORIENTED_EDGE('',*,*,#13225,.T.);
#17045=ORIENTED_EDGE('',*,*,#13218,.F.);
#17046=ORIENTED_EDGE('',*,*,#13226,.F.);
#17047=ORIENTED_EDGE('',*,*,#13223,.T.);
#17048=ORIENTED_EDGE('',*,*,#13217,.T.);
#17049=ORIENTED_EDGE('',*,*,#13221,.T.);
#17050=ORIENTED_EDGE('',*,*,#13224,.T.);
#17051=ORIENTED_EDGE('',*,*,#13226,.T.);
#17052=ORIENTED_EDGE('',*,*,#13199,.F.);
#17053=ORIENTED_EDGE('',*,*,#13202,.F.);
#17054=ORIENTED_EDGE('',*,*,#13205,.F.);
#17055=ORIENTED_EDGE('',*,*,#13208,.F.);
#17056=ORIENTED_EDGE('',*,*,#13211,.F.);
#17057=ORIENTED_EDGE('',*,*,#13214,.F.);
#17058=ORIENTED_EDGE('',*,*,#13215,.F.);
#17059=ORIENTED_EDGE('',*,*,#13225,.F.);
#17060=ORIENTED_EDGE('',*,*,#13222,.F.);
#17061=ORIENTED_EDGE('',*,*,#13219,.F.);
#17062=ORIENTED_EDGE('',*,*,#13197,.T.);
#17063=ORIENTED_EDGE('',*,*,#13200,.T.);
#17064=ORIENTED_EDGE('',*,*,#13203,.T.);
#17065=ORIENTED_EDGE('',*,*,#13206,.T.);
#17066=ORIENTED_EDGE('',*,*,#13209,.T.);
#17067=ORIENTED_EDGE('',*,*,#13212,.T.);
#23837=CYLINDRICAL_SURFACE('',#26204,3.3);
#23838=CYLINDRICAL_SURFACE('',#26207,3.3);
#23839=CYLINDRICAL_SURFACE('',#26210,3.3);
#23840=CYLINDRICAL_SURFACE('',#26213,3.3);
#23841=CYLINDRICAL_SURFACE('',#26216,3.3);
#23842=CYLINDRICAL_SURFACE('',#26219,3.3);
#24304=ADVANCED_FACE('',(#2351),#23837,.F.);
#24305=ADVANCED_FACE('',(#2352),#23838,.F.);
#24306=ADVANCED_FACE('',(#2353),#23839,.F.);
#24307=ADVANCED_FACE('',(#2354),#23840,.F.);
#24308=ADVANCED_FACE('',(#2355),#23841,.F.);
#24309=ADVANCED_FACE('',(#2356),#23842,.F.);
#24310=ADVANCED_FACE('',(#2357),#1545,.F.);
#24311=ADVANCED_FACE('',(#2358),#1546,.F.);
#24312=ADVANCED_FACE('',(#2359),#1547,.F.);
#24313=ADVANCED_FACE('',(#2360),#1548,.F.);
#24314=ADVANCED_FACE('',(#2361,#1235,#1236,#1237,#1238,#1239,#1240),#1549,
 .T.);
#24315=ADVANCED_FACE('',(#2362,#1241,#1242,#1243,#1244,#1245,#1246),#1550,
 .F.);
#25669=CLOSED_SHELL('',(#24304,#24305,#24306,#24307,#24308,#24309,#24310,
#24311,#24312,#24313,#24314,#24315));
#26203=AXIS2_PLACEMENT_3D('',#36612,#29217,#29218);
#26204=AXIS2_PLACEMENT_3D('',#36613,#29219,#29220);
#26205=AXIS2_PLACEMENT_3D('',#36615,#29221,#29222);
#26206=AXIS2_PLACEMENT_3D('',#36618,#29224,#29225);
#26207=AXIS2_PLACEMENT_3D('',#36619,#29226,#29227);
#26208=AXIS2_PLACEMENT_3D('',#36621,#29228,#29229);
#26209=AXIS2_PLACEMENT_3D('',#36624,#29231,#29232);
#26210=AXIS2_PLACEMENT_3D('',#36625,#29233,#29234);
#26211=AXIS2_PLACEMENT_3D('',#36627,#29235,#29236);
#26212=AXIS2_PLACEMENT_3D('',#36630,#29238,#29239);
#26213=AXIS2_PLACEMENT_3D('',#36631,#29240,#29241);
#26214=AXIS2_PLACEMENT_3D('',#36633,#29242,#29243);
#26215=AXIS2_PLACEMENT_3D('',#36636,#29245,#29246);
#26216=AXIS2_PLACEMENT_3D('',#36637,#29247,#29248);
#26217=AXIS2_PLACEMENT_3D('',#36639,#29249,#29250);
#26218=AXIS2_PLACEMENT_3D('',#36642,#29252,#29253);
#26219=AXIS2_PLACEMENT_3D('',#36643,#29254,#29255);
#26220=AXIS2_PLACEMENT_3D('',#36645,#29256,#29257);
#26221=AXIS2_PLACEMENT_3D('',#36648,#29259,#29260);
#26222=AXIS2_PLACEMENT_3D('',#36649,#29261,#29262);
#26223=AXIS2_PLACEMENT_3D('',#36658,#29267,#29268);
#26224=AXIS2_PLACEMENT_3D('',#36664,#29272,#29273);
#26225=AXIS2_PLACEMENT_3D('',#36670,#29277,#29278);
#26226=AXIS2_PLACEMENT_3D('',#36673,#29281,#29282);
#26227=AXIS2_PLACEMENT_3D('',#36674,#29283,#29284);
#29217=DIRECTION('axis',(0.,0.,1.));
#29218=DIRECTION('refdir',(1.,0.,0.));
#29219=DIRECTION('center_axis',(0.,0.,1.));
#29220=DIRECTION('ref_axis',(1.,0.,0.));
#29221=DIRECTION('center_axis',(0.,0.,1.));
#29222=DIRECTION('ref_axis',(1.,0.,0.));
#29223=DIRECTION('',(0.,0.,1.));
#29224=DIRECTION('center_axis',(0.,0.,1.));
#29225=DIRECTION('ref_axis',(1.,0.,0.));
#29226=DIRECTION('center_axis',(0.,0.,1.));
#29227=DIRECTION('ref_axis',(1.,0.,0.));
#29228=DIRECTION('center_axis',(0.,0.,1.));
#29229=DIRECTION('ref_axis',(1.,0.,0.));
#29230=DIRECTION('',(0.,0.,1.));
#29231=DIRECTION('center_axis',(0.,0.,1.));
#29232=DIRECTION('ref_axis',(1.,0.,0.));
#29233=DIRECTION('center_axis',(0.,0.,1.));
#29234=DIRECTION('ref_axis',(1.,0.,0.));
#29235=DIRECTION('center_axis',(0.,0.,1.));
#29236=DIRECTION('ref_axis',(1.,0.,0.));
#29237=DIRECTION('',(0.,0.,1.));
#29238=DIRECTION('center_axis',(0.,0.,1.));
#29239=DIRECTION('ref_axis',(1.,0.,0.));
#29240=DIRECTION('center_axis',(0.,0.,1.));
#29241=DIRECTION('ref_axis',(1.,0.,0.));
#29242=DIRECTION('center_axis',(0.,0.,1.));
#29243=DIRECTION('ref_axis',(1.,0.,0.));
#29244=DIRECTION('',(0.,0.,1.));
#29245=DIRECTION('center_axis',(0.,0.,1.));
#29246=DIRECTION('ref_axis',(1.,0.,0.));
#29247=DIRECTION('center_axis',(0.,0.,1.));
#29248=DIRECTION('ref_axis',(1.,0.,0.));
#29249=DIRECTION('center_axis',(0.,0.,1.));
#29250=DIRECTION('ref_axis',(1.,0.,0.));
#29251=DIRECTION('',(0.,0.,1.));
#29252=DIRECTION('center_axis',(0.,0.,1.));
#29253=DIRECTION('ref_axis',(1.,0.,0.));
#29254=DIRECTION('center_axis',(0.,0.,1.));
#29255=DIRECTION('ref_axis',(1.,0.,0.));
#29256=DIRECTION('center_axis',(0.,0.,1.));
#29257=DIRECTION('ref_axis',(1.,0.,0.));
#29258=DIRECTION('',(0.,0.,1.));
#29259=DIRECTION('center_axis',(0.,0.,1.));
#29260=DIRECTION('ref_axis',(1.,0.,0.));
#29261=DIRECTION('center_axis',(-1.,1.26161707343768E-16,0.));
#29262=DIRECTION('ref_axis',(-1.26161707343768E-16,-1.,0.));
#29263=DIRECTION('',(1.26161707343768E-16,1.,0.));
#29264=DIRECTION('',(0.,0.,-1.));
#29265=DIRECTION('',(1.26161707343768E-16,1.,0.));
#29266=DIRECTION('',(0.,0.,-1.));
#29267=DIRECTION('center_axis',(0.,-1.,0.));
#29268=DIRECTION('ref_axis',(0.,0.,-1.));
#29269=DIRECTION('',(-1.,0.,0.));
#29270=DIRECTION('',(0.,0.,-1.));
#29271=DIRECTION('',(-1.,0.,0.));
#29272=DIRECTION('center_axis',(1.,0.,0.));
#29273=DIRECTION('ref_axis',(0.,0.,-1.));
#29274=DIRECTION('',(0.,-1.,0.));
#29275=DIRECTION('',(0.,0.,-1.));
#29276=DIRECTION('',(0.,-1.,0.));
#29277=DIRECTION('center_axis',(0.,1.,0.));
#29278=DIRECTION('ref_axis',(0.,0.,1.));
#29279=DIRECTION('',(1.,0.,0.));
#29280=DIRECTION('',(1.,0.,0.));
#29281=DIRECTION('center_axis',(0.,0.,1.));
#29282=DIRECTION('ref_axis',(1.,0.,0.));
#29283=DIRECTION('center_axis',(0.,0.,1.));
#29284=DIRECTION('ref_axis',(1.,0.,0.));
#36612=CARTESIAN_POINT('',(0.,0.,0.));
#36613=CARTESIAN_POINT('Origin',(40.,33.,2.5));
#36614=CARTESIAN_POINT('',(36.7,33.,-2.5));
#36615=CARTESIAN_POINT('Origin',(40.,33.,-2.5));
#36616=CARTESIAN_POINT('',(36.7,33.,2.5));
#36617=CARTESIAN_POINT('',(36.7,33.,2.5));
#36618=CARTESIAN_POINT('Origin',(40.,33.,2.5));
#36619=CARTESIAN_POINT('Origin',(-40.,33.,2.5));
#36620=CARTESIAN_POINT('',(-43.3,33.,-2.5));
#36621=CARTESIAN_POINT('Origin',(-40.,33.,-2.5));
#36622=CARTESIAN_POINT('',(-43.3,33.,2.5));
#36623=CARTESIAN_POINT('',(-43.3,33.,2.5));
#36624=CARTESIAN_POINT('Origin',(-40.,33.,2.5));
#36625=CARTESIAN_POINT('Origin',(-40.,-33.,2.5));
#36626=CARTESIAN_POINT('',(-43.3,-33.,-2.5));
#36627=CARTESIAN_POINT('Origin',(-40.,-33.,-2.5));
#36628=CARTESIAN_POINT('',(-43.3,-33.,2.5));
#36629=CARTESIAN_POINT('',(-43.3,-33.,2.5));
#36630=CARTESIAN_POINT('Origin',(-40.,-33.,2.5));
#36631=CARTESIAN_POINT('Origin',(40.,-33.,2.5));
#36632=CARTESIAN_POINT('',(36.7,-33.,-2.5));
#36633=CARTESIAN_POINT('Origin',(40.,-33.,-2.5));
#36634=CARTESIAN_POINT('',(36.7,-33.,2.5));
#36635=CARTESIAN_POINT('',(36.7,-33.,2.5));
#36636=CARTESIAN_POINT('Origin',(40.,-33.,2.5));
#36637=CARTESIAN_POINT('Origin',(-20.,33.,2.5));
#36638=CARTESIAN_POINT('',(-23.3,33.,-2.5));
#36639=CARTESIAN_POINT('Origin',(-20.,33.,-2.5));
#36640=CARTESIAN_POINT('',(-23.3,33.,2.5));
#36641=CARTESIAN_POINT('',(-23.3,33.,2.5));
#36642=CARTESIAN_POINT('Origin',(-20.,33.,2.5));
#36643=CARTESIAN_POINT('Origin',(20.,-33.,2.5));
#36644=CARTESIAN_POINT('',(16.7,-33.,-2.5));
#36645=CARTESIAN_POINT('Origin',(20.,-33.,-2.5));
#36646=CARTESIAN_POINT('',(16.7,-33.,2.5));
#36647=CARTESIAN_POINT('',(16.7,-33.,2.5));
#36648=CARTESIAN_POINT('Origin',(20.,-33.,2.5));
#36649=CARTESIAN_POINT('Origin',(65.,55.,2.5));
#36650=CARTESIAN_POINT('',(65.,-55.,-2.5));
#36651=CARTESIAN_POINT('',(65.,55.,-2.5));
#36652=CARTESIAN_POINT('',(65.,55.,-2.5));
#36653=CARTESIAN_POINT('',(65.,55.,2.5));
#36654=CARTESIAN_POINT('',(65.,55.,2.5));
#36655=CARTESIAN_POINT('',(65.,-55.,2.5));
#36656=CARTESIAN_POINT('',(65.,55.,2.5));
#36657=CARTESIAN_POINT('',(65.,-55.,2.5));
#36658=CARTESIAN_POINT('Origin',(-65.,55.,2.5));
#36659=CARTESIAN_POINT('',(-65.,55.,-2.5));
#36660=CARTESIAN_POINT('',(-65.,55.,-2.5));
#36661=CARTESIAN_POINT('',(-65.,55.,2.5));
#36662=CARTESIAN_POINT('',(-65.,55.,2.5));
#36663=CARTESIAN_POINT('',(-65.,55.,2.5));
#36664=CARTESIAN_POINT('Origin',(-65.,55.,2.5));
#36665=CARTESIAN_POINT('',(-65.,-55.,-2.5));
#36666=CARTESIAN_POINT('',(-65.,55.,-2.5));
#36667=CARTESIAN_POINT('',(-65.,-55.,2.5));
#36668=CARTESIAN_POINT('',(-65.,-55.,2.5));
#36669=CARTESIAN_POINT('',(-65.,55.,2.5));
#36670=CARTESIAN_POINT('Origin',(-65.,-55.,2.5));
#36671=CARTESIAN_POINT('',(-65.,-55.,-2.5));
#36672=CARTESIAN_POINT('',(-65.,-55.,2.5));
#36673=CARTESIAN_POINT('Origin',(0.,0.,2.5));
#36674=CARTESIAN_POINT('Origin',(0.,0.,-2.5));
#66648=UNCERTAINTY_MEASURE_WITH_UNIT(LENGTH_MEASURE(0.01),#66722,
'DISTANCE_ACCURACY_VALUE',
'Maximum model space distance between geometric entities at asserted c
onnectivities');
#66680=UNCERTAINTY_MEASURE_WITH_UNIT(LENGTH_MEASURE(0.01),#66722,
'DISTANCE_ACCURACY_VALUE',
'Maximum model space distance between geometric entities at asserted c
onnectivities');
#66689=(
GEOMETRIC_REPRESENTATION_CONTEXT(3)
GLOBAL_UNCERTAINTY_ASSIGNED_CONTEXT((#66648))
GLOBAL_UNIT_ASSIGNED_CONTEXT((#66722,#66724,#66725))
REPRESENTATION_CONTEXT('','3D')
);
#66721=(
GEOMETRIC_REPRESENTATION_CONTEXT(3)
GLOBAL_UNCERTAINTY_ASSIGNED_CONTEXT((#66680))
GLOBAL_UNIT_ASSIGNED_CONTEXT((#66722,#66724,#66725))
REPRESENTATION_CONTEXT('','3D')
);
#66722=(
LENGTH_UNIT()
NAMED_UNIT(*)
SI_UNIT(.MILLI.,.METRE.)
);
#66724=(
NAMED_UNIT(*)
PLANE_ANGLE_UNIT()
SI_UNIT($,.RADIAN.)
);
#66725=(
NAMED_UNIT(*)
SI_UNIT($,.STERADIAN.)
SOLID_ANGLE_UNIT()
);
#66734=SHAPE_DEFINITION_REPRESENTATION(#66776,#66898);
#66776=PRODUCT_DEFINITION_SHAPE('',$,#66939);
#66898=SHAPE_REPRESENTATION('',(#26203),#66689);
#66930=PRODUCT_DEFINITION_CONTEXT('part definition',#67052,'design');
#66939=PRODUCT_DEFINITION('Ball Screw Support Spacer',
'Ball Screw Support Spacer',#66979,#66930);
#66979=PRODUCT_DEFINITION_FORMATION('',$,#67062);
#67052=APPLICATION_CONTEXT(
'Core Data for Automotive Mechanical Design Process');
#67053=PRODUCT_CONTEXT('part definition',#67052,'mechanical');
#67062=PRODUCT('Ball Screw Support Spacer','Ball Screw Support Spacer',
$,(#67053));
#67095=PRESENTATION_STYLE_ASSIGNMENT((#67097));
#67097=SURFACE_STYLE_USAGE(.BOTH.,#67099);
#67099=SURFACE_SIDE_STYLE('',(#67101));
#67101=SURFACE_STYLE_FILL_AREA(#67103);
#67103=FILL_AREA_STYLE('Opaque(202,209,238)',(#67105));
#67105=FILL_AREA_STYLE_COLOUR('Opaque(202,209,238)',#67107);
#67107=COLOUR_RGB('Opaque(202,209,238)',0.792156862745098,0.819607843137255,
0.933333333333333);
ENDSEC;
END-ISO-10303-21;
